ISO-10303-21;
HEADER;
/* Generated by software containing ST-Developer
 * from STEP Tools, Inc. (www.steptools.com) 
 */

FILE_DESCRIPTION(
/* description */ ('Cam-and-follower valve demonstrator'),
/* implementation_level */ '2;1');

FILE_NAME(
/* name */ 'Cap Screw - M4x16.step',
/* time_stamp */ '2026-10-28T03:25:17-07:00',
/* author */ (''),
/* organization */ (''),
/* preprocessor_version */ 'ST-DEVELOPER v20.2',
/* originating_system */ 'Autodesk Translation Framework v15.17.0.0',
/* authorisation */ '');

FILE_SCHEMA (('AUTOMOTIVE_DESIGN { 1 0 10303 214 3 1 1 }'));
ENDSEC;

DATA;
#10=MECHANICAL_DESIGN_GEOMETRIC_PRESENTATION_REPRESENTATION('',(#451),#12896);
#13=ORIENTED_CLOSED_SHELL('',*,#6221,.F.);
#16=BREP_WITH_VOIDS('Body1',#6220,(#13));
#318=CONICAL_SURFACE('',#7295,0.325,0.785398163397448);
#319=CONICAL_SURFACE('',#7299,0.335,0.785398163397448);
#320=CONICAL_SURFACE('',#7303,0.21,0.463647609000806);
#321=CONICAL_SURFACE('',#7307,0.18,0.785398163397448);
#372=SHAPE_REPRESENTATION_RELATIONSHIP('SRR','None',#13091,#408);
#408=ADVANCED_BREP_SHAPE_REPRESENTATION('',(#16),#12891);
#451=STYLED_ITEM('',(#13337),#16);
#652=FACE_BOUND('',#1958,.T.);
#953=CIRCLE('',#7294,0.3);
#954=CIRCLE('',#7296,0.35);
#955=CIRCLE('',#7298,0.35);
#956=CIRCLE('',#7300,0.32);
#957=CIRCLE('',#7302,0.22);
#958=CIRCLE('',#7304,0.1954);
#959=CIRCLE('',#7306,0.1954);
#960=CIRCLE('',#7308,0.16);
#1087=CYLINDRICAL_SURFACE('',#7297,0.35);
#1088=CYLINDRICAL_SURFACE('',#7305,0.1954);
#1428=FACE_OUTER_BOUND('',#1953,.T.);
#1429=FACE_OUTER_BOUND('',#1954,.T.);
#1430=FACE_OUTER_BOUND('',#1955,.T.);
#1431=FACE_OUTER_BOUND('',#1956,.T.);
#1432=FACE_OUTER_BOUND('',#1957,.T.);
#1433=FACE_OUTER_BOUND('',#1959,.T.);
#1434=FACE_OUTER_BOUND('',#1960,.T.);
#1435=FACE_OUTER_BOUND('',#1961,.T.);
#1436=FACE_OUTER_BOUND('',#1962,.T.);
#1437=FACE_OUTER_BOUND('',#1963,.T.);
#1438=FACE_OUTER_BOUND('',#1964,.T.);
#1439=FACE_OUTER_BOUND('',#1965,.T.);
#1440=FACE_OUTER_BOUND('',#1966,.T.);
#1441=FACE_OUTER_BOUND('',#1967,.T.);
#1442=FACE_OUTER_BOUND('',#1968,.T.);
#1443=FACE_OUTER_BOUND('',#1969,.T.);
#1444=FACE_OUTER_BOUND('',#1970,.T.);
#1953=EDGE_LOOP('',(#5473));
#1954=EDGE_LOOP('',(#5474,#5475,#5476,#5477));
#1955=EDGE_LOOP('',(#5478,#5479,#5480,#5481));
#1956=EDGE_LOOP('',(#5482,#5483,#5484,#5485));
#1957=EDGE_LOOP('',(#5486));
#1958=EDGE_LOOP('',(#5487));
#1959=EDGE_LOOP('',(#5488,#5489,#5490,#5491));
#1960=EDGE_LOOP('',(#5492,#5493,#5494,#5495));
#1961=EDGE_LOOP('',(#5496,#5497,#5498,#5499));
#1962=EDGE_LOOP('',(#5500));
#1963=EDGE_LOOP('',(#5501,#5502,#5503,#5504));
#1964=EDGE_LOOP('',(#5505,#5506,#5507,#5508));
#1965=EDGE_LOOP('',(#5509,#5510,#5511,#5512));
#1966=EDGE_LOOP('',(#5513,#5514,#5515,#5516));
#1967=EDGE_LOOP('',(#5517,#5518,#5519,#5520));
#1968=EDGE_LOOP('',(#5521,#5522,#5523,#5524));
#1969=EDGE_LOOP('',(#5525,#5526,#5527,#5528,#5529,#5530));
#1970=EDGE_LOOP('',(#5531,#5532,#5533,#5534,#5535,#5536));
#2375=LINE('',#12614,#2797);
#2376=LINE('',#12618,#2798);
#2377=LINE('',#12622,#2799);
#2378=LINE('',#12629,#2800);
#2379=LINE('',#12633,#2801);
#2380=LINE('',#12637,#2802);
#2381=LINE('',#12642,#2803);
#2382=LINE('',#12644,#2804);
#2383=LINE('',#12646,#2805);
#2384=LINE('',#12647,#2806);
#2385=LINE('',#12650,#2807);
#2386=LINE('',#12652,#2808);
#2387=LINE('',#12653,#2809);
#2388=LINE('',#12656,#2810);
#2389=LINE('',#12658,#2811);
#2390=LINE('',#12659,#2812);
#2391=LINE('',#12662,#2813);
#2392=LINE('',#12664,#2814);
#2393=LINE('',#12665,#2815);
#2394=LINE('',#12668,#2816);
#2395=LINE('',#12670,#2817);
#2396=LINE('',#12671,#2818);
#2397=LINE('',#12673,#2819);
#2398=LINE('',#12674,#2820);
#2797=VECTOR('',#9144,0.325);
#2798=VECTOR('',#9149,0.35);
#2799=VECTOR('',#9154,0.335);
#2800=VECTOR('',#9163,0.21);
#2801=VECTOR('',#9168,0.2);
#2802=VECTOR('',#9173,0.18);
#2803=VECTOR('',#9178,1.);
#2804=VECTOR('',#9179,1.);
#2805=VECTOR('',#9180,1.);
#2806=VECTOR('',#9181,1.);
#2807=VECTOR('',#9184,1.);
#2808=VECTOR('',#9185,1.);
#2809=VECTOR('',#9186,1.);
#2810=VECTOR('',#9189,1.);
#2811=VECTOR('',#9190,1.);
#2812=VECTOR('',#9191,1.);
#2813=VECTOR('',#9194,1.);
#2814=VECTOR('',#9195,1.);
#2815=VECTOR('',#9196,1.);
#2816=VECTOR('',#9199,1.);
#2817=VECTOR('',#9200,1.);
#2818=VECTOR('',#9201,1.);
#2819=VECTOR('',#9204,1.);
#2820=VECTOR('',#9205,1.);
#3304=VERTEX_POINT('',#12609);
#3305=VERTEX_POINT('',#12612);
#3306=VERTEX_POINT('',#12616);
#3307=VERTEX_POINT('',#12620);
#3308=VERTEX_POINT('',#12624);
#3309=VERTEX_POINT('',#12627);
#3310=VERTEX_POINT('',#12631);
#3311=VERTEX_POINT('',#12635);
#3312=VERTEX_POINT('',#12640);
#3313=VERTEX_POINT('',#12641);
#3314=VERTEX_POINT('',#12643);
#3315=VERTEX_POINT('',#12645);
#3316=VERTEX_POINT('',#12649);
#3317=VERTEX_POINT('',#12651);
#3318=VERTEX_POINT('',#12655);
#3319=VERTEX_POINT('',#12657);
#3320=VERTEX_POINT('',#12661);
#3321=VERTEX_POINT('',#12663);
#3322=VERTEX_POINT('',#12667);
#3323=VERTEX_POINT('',#12669);
#4033=EDGE_CURVE('',#3304,#3304,#953,.T.);
#4034=EDGE_CURVE('',#3305,#3305,#954,.T.);
#4035=EDGE_CURVE('',#3305,#3304,#2375,.T.);
#4036=EDGE_CURVE('',#3306,#3306,#955,.T.);
#4037=EDGE_CURVE('',#3306,#3305,#2376,.T.);
#4038=EDGE_CURVE('',#3307,#3307,#956,.T.);
#4039=EDGE_CURVE('',#3307,#3306,#2377,.T.);
#4040=EDGE_CURVE('',#3308,#3308,#957,.T.);
#4041=EDGE_CURVE('',#3309,#3309,#958,.F.);
#4042=EDGE_CURVE('',#3309,#3308,#2378,.T.);
#4043=EDGE_CURVE('',#3310,#3310,#959,.F.);
#4044=EDGE_CURVE('',#3310,#3309,#2379,.T.);
#4045=EDGE_CURVE('',#3311,#3311,#960,.T.);
#4046=EDGE_CURVE('',#3311,#3310,#2380,.T.);
#4047=EDGE_CURVE('',#3312,#3313,#2381,.T.);
#4048=EDGE_CURVE('',#3313,#3314,#2382,.T.);
#4049=EDGE_CURVE('',#3314,#3315,#2383,.T.);
#4050=EDGE_CURVE('',#3312,#3315,#2384,.T.);
#4051=EDGE_CURVE('',#3313,#3316,#2385,.T.);
#4052=EDGE_CURVE('',#3316,#3317,#2386,.T.);
#4053=EDGE_CURVE('',#3317,#3314,#2387,.T.);
#4054=EDGE_CURVE('',#3316,#3318,#2388,.T.);
#4055=EDGE_CURVE('',#3318,#3319,#2389,.T.);
#4056=EDGE_CURVE('',#3319,#3317,#2390,.T.);
#4057=EDGE_CURVE('',#3318,#3320,#2391,.T.);
#4058=EDGE_CURVE('',#3320,#3321,#2392,.T.);
#4059=EDGE_CURVE('',#3321,#3319,#2393,.T.);
#4060=EDGE_CURVE('',#3320,#3322,#2394,.T.);
#4061=EDGE_CURVE('',#3322,#3323,#2395,.T.);
#4062=EDGE_CURVE('',#3323,#3321,#2396,.T.);
#4063=EDGE_CURVE('',#3322,#3312,#2397,.T.);
#4064=EDGE_CURVE('',#3315,#3323,#2398,.T.);
#5473=ORIENTED_EDGE('',*,*,#4033,.F.);
#5474=ORIENTED_EDGE('',*,*,#4034,.F.);
#5475=ORIENTED_EDGE('',*,*,#4035,.T.);
#5476=ORIENTED_EDGE('',*,*,#4033,.T.);
#5477=ORIENTED_EDGE('',*,*,#4035,.F.);
#5478=ORIENTED_EDGE('',*,*,#4036,.F.);
#5479=ORIENTED_EDGE('',*,*,#4037,.T.);
#5480=ORIENTED_EDGE('',*,*,#4034,.T.);
#5481=ORIENTED_EDGE('',*,*,#4037,.F.);
#5482=ORIENTED_EDGE('',*,*,#4038,.F.);
#5483=ORIENTED_EDGE('',*,*,#4039,.T.);
#5484=ORIENTED_EDGE('',*,*,#4036,.T.);
#5485=ORIENTED_EDGE('',*,*,#4039,.F.);
#5486=ORIENTED_EDGE('',*,*,#4038,.T.);
#5487=ORIENTED_EDGE('',*,*,#4040,.F.);
#5488=ORIENTED_EDGE('',*,*,#4041,.F.);
#5489=ORIENTED_EDGE('',*,*,#4042,.T.);
#5490=ORIENTED_EDGE('',*,*,#4040,.T.);
#5491=ORIENTED_EDGE('',*,*,#4042,.F.);
#5492=ORIENTED_EDGE('',*,*,#4043,.F.);
#5493=ORIENTED_EDGE('',*,*,#4044,.T.);
#5494=ORIENTED_EDGE('',*,*,#4041,.T.);
#5495=ORIENTED_EDGE('',*,*,#4044,.F.);
#5496=ORIENTED_EDGE('',*,*,#4045,.F.);
#5497=ORIENTED_EDGE('',*,*,#4046,.T.);
#5498=ORIENTED_EDGE('',*,*,#4043,.T.);
#5499=ORIENTED_EDGE('',*,*,#4046,.F.);
#5500=ORIENTED_EDGE('',*,*,#4045,.T.);
#5501=ORIENTED_EDGE('',*,*,#4047,.T.);
#5502=ORIENTED_EDGE('',*,*,#4048,.T.);
#5503=ORIENTED_EDGE('',*,*,#4049,.T.);
#5504=ORIENTED_EDGE('',*,*,#4050,.F.);
#5505=ORIENTED_EDGE('',*,*,#4051,.T.);
#5506=ORIENTED_EDGE('',*,*,#4052,.T.);
#5507=ORIENTED_EDGE('',*,*,#4053,.T.);
#5508=ORIENTED_EDGE('',*,*,#4048,.F.);
#5509=ORIENTED_EDGE('',*,*,#4054,.T.);
#5510=ORIENTED_EDGE('',*,*,#4055,.T.);
#5511=ORIENTED_EDGE('',*,*,#4056,.T.);
#5512=ORIENTED_EDGE('',*,*,#4052,.F.);
#5513=ORIENTED_EDGE('',*,*,#4057,.T.);
#5514=ORIENTED_EDGE('',*,*,#4058,.T.);
#5515=ORIENTED_EDGE('',*,*,#4059,.T.);
#5516=ORIENTED_EDGE('',*,*,#4055,.F.);
#5517=ORIENTED_EDGE('',*,*,#4060,.T.);
#5518=ORIENTED_EDGE('',*,*,#4061,.T.);
#5519=ORIENTED_EDGE('',*,*,#4062,.T.);
#5520=ORIENTED_EDGE('',*,*,#4058,.F.);
#5521=ORIENTED_EDGE('',*,*,#4063,.T.);
#5522=ORIENTED_EDGE('',*,*,#4050,.T.);
#5523=ORIENTED_EDGE('',*,*,#4064,.T.);
#5524=ORIENTED_EDGE('',*,*,#4061,.F.);
#5525=ORIENTED_EDGE('',*,*,#4063,.F.);
#5526=ORIENTED_EDGE('',*,*,#4060,.F.);
#5527=ORIENTED_EDGE('',*,*,#4057,.F.);
#5528=ORIENTED_EDGE('',*,*,#4054,.F.);
#5529=ORIENTED_EDGE('',*,*,#4051,.F.);
#5530=ORIENTED_EDGE('',*,*,#4047,.F.);
#5531=ORIENTED_EDGE('',*,*,#4064,.F.);
#5532=ORIENTED_EDGE('',*,*,#4049,.F.);
#5533=ORIENTED_EDGE('',*,*,#4053,.F.);
#5534=ORIENTED_EDGE('',*,*,#4056,.F.);
#5535=ORIENTED_EDGE('',*,*,#4059,.F.);
#5536=ORIENTED_EDGE('',*,*,#4062,.F.);
#5788=PLANE('',#7293);
#5789=PLANE('',#7301);
#5790=PLANE('',#7309);
#5791=PLANE('',#7310);
#5792=PLANE('',#7311);
#5793=PLANE('',#7312);
#5794=PLANE('',#7313);
#5795=PLANE('',#7314);
#5796=PLANE('',#7315);
#5797=PLANE('',#7316);
#5798=PLANE('',#7317);
#6144=ADVANCED_FACE('',(#1428),#5788,.T.);
#6145=ADVANCED_FACE('',(#1429),#318,.T.);
#6146=ADVANCED_FACE('',(#1430),#1087,.T.);
#6147=ADVANCED_FACE('',(#1431),#319,.T.);
#6148=ADVANCED_FACE('',(#1432,#652),#5789,.T.);
#6149=ADVANCED_FACE('',(#1433),#320,.T.);
#6150=ADVANCED_FACE('',(#1434),#1088,.T.);
#6151=ADVANCED_FACE('',(#1435),#321,.T.);
#6152=ADVANCED_FACE('',(#1436),#5790,.T.);
#6153=ADVANCED_FACE('',(#1437),#5791,.F.);
#6154=ADVANCED_FACE('',(#1438),#5792,.F.);
#6155=ADVANCED_FACE('',(#1439),#5793,.F.);
#6156=ADVANCED_FACE('',(#1440),#5794,.F.);
#6157=ADVANCED_FACE('',(#1441),#5795,.F.);
#6158=ADVANCED_FACE('',(#1442),#5796,.F.);
#6159=ADVANCED_FACE('',(#1443),#5797,.F.);
#6160=ADVANCED_FACE('',(#1444),#5798,.F.);
#6220=CLOSED_SHELL('',(#6144,#6145,#6146,#6147,#6148,#6149,#6150,#6151,
#6152));
#6221=CLOSED_SHELL('',(#6153,#6154,#6155,#6156,#6157,#6158,#6159,#6160));
#7292=AXIS2_PLACEMENT_3D('',#12607,#9134,#9135);
#7293=AXIS2_PLACEMENT_3D('',#12608,#9136,#9137);
#7294=AXIS2_PLACEMENT_3D('',#12610,#9138,#9139);
#7295=AXIS2_PLACEMENT_3D('',#12611,#9140,#9141);
#7296=AXIS2_PLACEMENT_3D('',#12613,#9142,#9143);
#7297=AXIS2_PLACEMENT_3D('',#12615,#9145,#9146);
#7298=AXIS2_PLACEMENT_3D('',#12617,#9147,#9148);
#7299=AXIS2_PLACEMENT_3D('',#12619,#9150,#9151);
#7300=AXIS2_PLACEMENT_3D('',#12621,#9152,#9153);
#7301=AXIS2_PLACEMENT_3D('',#12623,#9155,#9156);
#7302=AXIS2_PLACEMENT_3D('',#12625,#9157,#9158);
#7303=AXIS2_PLACEMENT_3D('',#12626,#9159,#9160);
#7304=AXIS2_PLACEMENT_3D('',#12628,#9161,#9162);
#7305=AXIS2_PLACEMENT_3D('',#12630,#9164,#9165);
#7306=AXIS2_PLACEMENT_3D('',#12632,#9166,#9167);
#7307=AXIS2_PLACEMENT_3D('',#12634,#9169,#9170);
#7308=AXIS2_PLACEMENT_3D('',#12636,#9171,#9172);
#7309=AXIS2_PLACEMENT_3D('',#12638,#9174,#9175);
#7310=AXIS2_PLACEMENT_3D('',#12639,#9176,#9177);
#7311=AXIS2_PLACEMENT_3D('',#12648,#9182,#9183);
#7312=AXIS2_PLACEMENT_3D('',#12654,#9187,#9188);
#7313=AXIS2_PLACEMENT_3D('',#12660,#9192,#9193);
#7314=AXIS2_PLACEMENT_3D('',#12666,#9197,#9198);
#7315=AXIS2_PLACEMENT_3D('',#12672,#9202,#9203);
#7316=AXIS2_PLACEMENT_3D('',#12675,#9206,#9207);
#7317=AXIS2_PLACEMENT_3D('',#12676,#9208,#9209);
#9134=DIRECTION('axis',(0.,0.,1.));
#9135=DIRECTION('refdir',(1.,0.,0.));
#9136=DIRECTION('center_axis',(0.,1.,0.));
#9137=DIRECTION('ref_axis',(0.,0.,1.));
#9138=DIRECTION('center_axis',(0.,-1.,0.));
#9139=DIRECTION('ref_axis',(1.,0.,0.));
#9140=DIRECTION('center_axis',(0.,-1.,0.));
#9141=DIRECTION('ref_axis',(1.,0.,0.));
#9142=DIRECTION('center_axis',(0.,-1.,0.));
#9143=DIRECTION('ref_axis',(1.,0.,0.));
#9144=DIRECTION('',(0.707106781186547,0.707106781186548,8.65956056235493E-17));
#9145=DIRECTION('center_axis',(0.,-1.,0.));
#9146=DIRECTION('ref_axis',(1.,0.,0.));
#9147=DIRECTION('center_axis',(0.,-1.,0.));
#9148=DIRECTION('ref_axis',(1.,0.,0.));
#9149=DIRECTION('',(0.,1.,0.));
#9150=DIRECTION('center_axis',(0.,1.,0.));
#9151=DIRECTION('ref_axis',(1.,0.,0.));
#9152=DIRECTION('center_axis',(0.,-1.,0.));
#9153=DIRECTION('ref_axis',(1.,0.,0.));
#9154=DIRECTION('',(-0.707106781186547,0.707106781186548,-8.65956056235493E-17));
#9155=DIRECTION('center_axis',(0.,-1.,0.));
#9156=DIRECTION('ref_axis',(0.,0.,-1.));
#9157=DIRECTION('center_axis',(0.,-1.,0.));
#9158=DIRECTION('ref_axis',(1.,0.,0.));
#9159=DIRECTION('center_axis',(0.,1.,0.));
#9160=DIRECTION('ref_axis',(1.,0.,0.));
#9161=DIRECTION('center_axis',(0.,1.,0.));
#9162=DIRECTION('ref_axis',(1.,0.,0.));
#9163=DIRECTION('',(-0.447213595499958,0.894427190999916,-5.47678698264203E-17));
#9164=DIRECTION('center_axis',(0.,-1.,0.));
#9165=DIRECTION('ref_axis',(1.,0.,0.));
#9166=DIRECTION('center_axis',(0.,1.,0.));
#9167=DIRECTION('ref_axis',(1.,0.,0.));
#9168=DIRECTION('',(0.,1.,0.));
#9169=DIRECTION('center_axis',(0.,1.,0.));
#9170=DIRECTION('ref_axis',(1.,0.,0.));
#9171=DIRECTION('center_axis',(0.,-1.,0.));
#9172=DIRECTION('ref_axis',(1.,0.,0.));
#9173=DIRECTION('',(-0.707106781186547,0.707106781186548,-8.65956056235493E-17));
#9174=DIRECTION('center_axis',(0.,-1.,0.));
#9175=DIRECTION('ref_axis',(0.,0.,-1.));
#9176=DIRECTION('center_axis',(0.866025403784439,0.,-0.5));
#9177=DIRECTION('ref_axis',(0.5,0.,0.866025403784439));
#9178=DIRECTION('',(-0.5,0.,-0.866025403784439));
#9179=DIRECTION('',(0.,-1.,0.));
#9180=DIRECTION('',(0.5,0.,0.866025403784439));
#9181=DIRECTION('',(0.,-1.,0.));
#9182=DIRECTION('center_axis',(1.60246890531964E-16,0.,-1.));
#9183=DIRECTION('ref_axis',(1.,0.,1.60246890531964E-16));
#9184=DIRECTION('',(-1.,0.,-1.60246890531964E-16));
#9185=DIRECTION('',(0.,-1.,0.));
#9186=DIRECTION('',(1.,0.,1.60246890531964E-16));
#9187=DIRECTION('center_axis',(-0.866025403784439,0.,-0.5));
#9188=DIRECTION('ref_axis',(0.5,0.,-0.866025403784439));
#9189=DIRECTION('',(-0.5,0.,0.866025403784439));
#9190=DIRECTION('',(0.,-1.,0.));
#9191=DIRECTION('',(0.5,0.,-0.866025403784439));
#9192=DIRECTION('center_axis',(-0.866025403784439,0.,0.5));
#9193=DIRECTION('ref_axis',(-0.5,0.,-0.866025403784439));
#9194=DIRECTION('',(0.5,0.,0.866025403784439));
#9195=DIRECTION('',(0.,-1.,0.));
#9196=DIRECTION('',(-0.5,0.,-0.866025403784439));
#9197=DIRECTION('center_axis',(-1.60246890531964E-16,0.,1.));
#9198=DIRECTION('ref_axis',(-1.,0.,-1.60246890531964E-16));
#9199=DIRECTION('',(1.,0.,1.60246890531964E-16));
#9200=DIRECTION('',(0.,-1.,0.));
#9201=DIRECTION('',(-1.,0.,-1.60246890531964E-16));
#9202=DIRECTION('center_axis',(0.866025403784439,0.,0.5));
#9203=DIRECTION('ref_axis',(-0.5,0.,0.866025403784439));
#9204=DIRECTION('',(0.5,0.,-0.866025403784439));
#9205=DIRECTION('',(-0.5,0.,0.866025403784439));
#9206=DIRECTION('center_axis',(0.,1.,0.));
#9207=DIRECTION('ref_axis',(1.,0.,0.));
#9208=DIRECTION('center_axis',(0.,-1.,0.));
#9209=DIRECTION('ref_axis',(0.,0.,-1.));
#12607=CARTESIAN_POINT('',(0.,0.,0.));
#12608=CARTESIAN_POINT('Origin',(0.3,0.4,0.));
#12609=CARTESIAN_POINT('',(-0.3,0.4,-3.67394039744206E-17));
#12610=CARTESIAN_POINT('Origin',(0.,0.4,0.));
#12611=CARTESIAN_POINT('Origin',(0.,0.375,0.));
#12612=CARTESIAN_POINT('',(-0.35,0.35,-4.28626379701573E-17));
#12613=CARTESIAN_POINT('Origin',(0.,0.35,0.));
#12614=CARTESIAN_POINT('',(-0.325,0.375,-3.9801020972289E-17));
#12615=CARTESIAN_POINT('Origin',(0.,0.19,0.));
#12616=CARTESIAN_POINT('',(-0.35,0.03,-4.28626379701574E-17));
#12617=CARTESIAN_POINT('Origin',(0.,0.03,0.));
#12618=CARTESIAN_POINT('',(-0.35,0.19,-4.28626379701574E-17));
#12619=CARTESIAN_POINT('Origin',(0.,0.0149999999999999,0.));
#12620=CARTESIAN_POINT('',(-0.32,-3.29597460435593E-17,-3.91886975727153E-17));
#12621=CARTESIAN_POINT('Origin',(0.,0.,0.));
#12622=CARTESIAN_POINT('',(-0.335,0.0149999999999999,-4.10256677714363E-17));
#12623=CARTESIAN_POINT('Origin',(0.22,0.,0.));
#12624=CARTESIAN_POINT('',(-0.22,-6.93889390390723E-18,-2.69422295812418E-17));
#12625=CARTESIAN_POINT('Origin',(0.,0.,0.));
#12626=CARTESIAN_POINT('Origin',(0.,-0.02,0.));
#12627=CARTESIAN_POINT('',(-0.1954,-0.0492,2.39295984553393E-17));
#12628=CARTESIAN_POINT('Origin',(0.,-0.0492,0.));
#12629=CARTESIAN_POINT('',(-0.21,-0.02,-2.57175827820944E-17));
#12630=CARTESIAN_POINT('Origin',(0.,-0.8,0.));
#12631=CARTESIAN_POINT('',(-0.1954,-1.5646,2.39295984553393E-17));
#12632=CARTESIAN_POINT('Origin',(0.,-1.5646,0.));
#12633=CARTESIAN_POINT('',(-0.1954,-0.8,-2.39295984553393E-17));
#12634=CARTESIAN_POINT('Origin',(0.,-1.58,0.));
#12635=CARTESIAN_POINT('',(-0.16,-1.6,-1.95943487863577E-17));
#12636=CARTESIAN_POINT('Origin',(0.,-1.6,0.));
#12637=CARTESIAN_POINT('',(-0.18,-1.58,-2.20436423846524E-17));
#12638=CARTESIAN_POINT('Origin',(0.,-1.6,0.));
#12639=CARTESIAN_POINT('Origin',(0.0866025403784439,-0.4,-0.15));
#12640=CARTESIAN_POINT('',(0.173205080756888,-0.4,0.));
#12641=CARTESIAN_POINT('',(0.0866025403784439,-0.4,-0.15));
#12642=CARTESIAN_POINT('',(0.173205080756888,-0.4,0.));
#12643=CARTESIAN_POINT('',(0.0866025403784439,-0.64,-0.15));
#12644=CARTESIAN_POINT('',(0.0866025403784439,-0.4,-0.15));
#12645=CARTESIAN_POINT('',(0.173205080756888,-0.64,0.));
#12646=CARTESIAN_POINT('',(0.173205080756888,-0.64,0.));
#12647=CARTESIAN_POINT('',(0.173205080756888,-0.4,0.));
#12648=CARTESIAN_POINT('Origin',(-0.0866025403784438,-0.4,-0.15));
#12649=CARTESIAN_POINT('',(-0.0866025403784438,-0.4,-0.15));
#12650=CARTESIAN_POINT('',(0.0866025403784439,-0.4,-0.15));
#12651=CARTESIAN_POINT('',(-0.0866025403784438,-0.64,-0.15));
#12652=CARTESIAN_POINT('',(-0.0866025403784438,-0.4,-0.15));
#12653=CARTESIAN_POINT('',(0.0866025403784439,-0.64,-0.15));
#12654=CARTESIAN_POINT('Origin',(-0.173205080756888,-0.4,-2.77555756156289E-17));
#12655=CARTESIAN_POINT('',(-0.173205080756888,-0.4,-2.12115047744981E-17));
#12656=CARTESIAN_POINT('',(-0.0866025403784438,-0.4,-0.15));
#12657=CARTESIAN_POINT('',(-0.173205080756888,-0.64,-2.77555756156289E-17));
#12658=CARTESIAN_POINT('',(-0.173205080756888,-0.4,-2.12115047744981E-17));
#12659=CARTESIAN_POINT('',(-0.0866025403784438,-0.64,-0.15));
#12660=CARTESIAN_POINT('Origin',(-0.0866025403784439,-0.4,0.15));
#12661=CARTESIAN_POINT('',(-0.0866025403784439,-0.4,0.15));
#12662=CARTESIAN_POINT('',(-0.173205080756888,-0.4,-2.12115047744981E-17));
#12663=CARTESIAN_POINT('',(-0.0866025403784439,-0.64,0.15));
#12664=CARTESIAN_POINT('',(-0.0866025403784439,-0.4,0.15));
#12665=CARTESIAN_POINT('',(-0.173205080756888,-0.64,-2.12115047744981E-17));
#12666=CARTESIAN_POINT('Origin',(0.0866025403784439,-0.4,0.15));
#12667=CARTESIAN_POINT('',(0.0866025403784439,-0.4,0.15));
#12668=CARTESIAN_POINT('',(-0.0866025403784439,-0.4,0.15));
#12669=CARTESIAN_POINT('',(0.0866025403784439,-0.64,0.15));
#12670=CARTESIAN_POINT('',(0.0866025403784439,-0.4,0.15));
#12671=CARTESIAN_POINT('',(-0.0866025403784439,-0.64,0.15));
#12672=CARTESIAN_POINT('Origin',(0.173205080756888,-0.4,0.));
#12673=CARTESIAN_POINT('',(0.0866025403784439,-0.4,0.15));
#12674=CARTESIAN_POINT('',(0.0866025403784439,-0.64,0.15));
#12675=CARTESIAN_POINT('Origin',(0.,-0.4,-2.77555756156289E-17));
#12676=CARTESIAN_POINT('Origin',(0.,-0.64,-2.77555756156289E-17));
#12848=UNCERTAINTY_MEASURE_WITH_UNIT(LENGTH_MEASURE(0.001),#12897,
'DISTANCE_ACCURACY_VALUE',
'Maximum model space distance between geometric entities at asserted c
onnectivities');
#12853=UNCERTAINTY_MEASURE_WITH_UNIT(LENGTH_MEASURE(0.001),#12897,
'DISTANCE_ACCURACY_VALUE',
'Maximum model space distance between geometric entities at asserted c
onnectivities');
#12891=(
GEOMETRIC_REPRESENTATION_CONTEXT(3)
GLOBAL_UNCERTAINTY_ASSIGNED_CONTEXT((#12848))
GLOBAL_UNIT_ASSIGNED_CONTEXT((#12897,#12899,#12900))
REPRESENTATION_CONTEXT('','3D')
);
#12896=(
GEOMETRIC_REPRESENTATION_CONTEXT(3)
GLOBAL_UNCERTAINTY_ASSIGNED_CONTEXT((#12853))
GLOBAL_UNIT_ASSIGNED_CONTEXT((#12897,#12899,#12900))
REPRESENTATION_CONTEXT('','3D')
);
#12897=(
LENGTH_UNIT()
NAMED_UNIT(*)
SI_UNIT(.CENTI.,.METRE.)
);
#12899=(
NAMED_UNIT(*)
PLANE_ANGLE_UNIT()
SI_UNIT($,.RADIAN.)
);
#12900=(
NAMED_UNIT(*)
SI_UNIT($,.STERADIAN.)
SOLID_ANGLE_UNIT()
);
#12938=SHAPE_DEFINITION_REPRESENTATION(#12987,#13091);
#12987=PRODUCT_DEFINITION_SHAPE('',$,#13134);
#13091=SHAPE_REPRESENTATION('',(#7292),#12891);
#13096=PRODUCT_DEFINITION_CONTEXT('part definition',#13224,'design');
#13134=PRODUCT_DEFINITION('Cap Screw - M4x16','Cap Screw - M4x16',#13176,
#13096);
#13176=PRODUCT_DEFINITION_FORMATION('',$,#13263);
#13224=APPLICATION_CONTEXT(
'Core Data for Automotive Mechanical Design Process');
#13225=PRODUCT_CONTEXT('part definition',#13224,'mechanical');
#13263=PRODUCT('Cap Screw - M4x16','Cap Screw - M4x16',
'Cap Screw - M4x16',(#13225));
#13331=COLOUR_RGB('Black',0.12,0.14,0.17);
#13332=FILL_AREA_STYLE_COLOUR('',#13331);
#13333=FILL_AREA_STYLE('',(#13332));
#13334=SURFACE_STYLE_FILL_AREA(#13333);
#13335=SURFACE_SIDE_STYLE('',(#13334));
#13336=SURFACE_STYLE_USAGE(.BOTH.,#13335);
#13337=PRESENTATION_STYLE_ASSIGNMENT((#13336));
ENDSEC;
END-ISO-10303-21;
